ISO-10303-21;
HEADER;
/* Generated by software containing ST-Developer
 * from STEP Tools, Inc. (www.steptools.com) 
 */

FILE_DESCRIPTION(
/* description */ (''),
/* implementation_level */ '2;1');

FILE_NAME(
/* name */ '11_Body_Face_Seal_O-Ring.step',
/* time_stamp */ '2026-10-26T06:59:52-07:00',
/* author */ (''),
/* organization */ (''),
/* preprocessor_version */ 'ST-DEVELOPER v20.2',
/* originating_system */ 'Autodesk Translation Framework v15.15.0.0',
/* authorisation */ '');

FILE_SCHEMA (('AUTOMOTIVE_DESIGN { 1 0 10303 214 3 1 1 }'));
ENDSEC;

DATA;
#10=MECHANICAL_DESIGN_GEOMETRIC_PRESENTATION_REPRESENTATION('',(#173),#46395);
#145=SHAPE_REPRESENTATION_RELATIONSHIP('SRR','None',#46465,#159);
#159=ADVANCED_BREP_SHAPE_REPRESENTATION('',(#187),#46390);
#173=STYLED_ITEM('',(#46603),#187);
#187=MANIFOLD_SOLID_BREP('Body1',#24946);
#233=TOROIDAL_SURFACE('',#26514,23.5,1.);
#234=TOROIDAL_SURFACE('',#26523,23.5,1.);
#530=CYLINDRICAL_SURFACE('',#26520,1.);
#531=CYLINDRICAL_SURFACE('',#26527,1.);
#2806=FACE_OUTER_BOUND('',#4216,.T.);
#2807=FACE_OUTER_BOUND('',#4217,.T.);
#2808=FACE_OUTER_BOUND('',#4218,.T.);
#2809=FACE_OUTER_BOUND('',#4219,.T.);
#4216=EDGE_LOOP('',(#22298,#22299,#22300,#22301,#22302,#22303));
#4217=EDGE_LOOP('',(#22304,#22305,#22306,#22307,#22308,#22309));
#4218=EDGE_LOOP('',(#22310,#22311,#22312,#22313,#22314,#22315));
#4219=EDGE_LOOP('',(#22316,#22317,#22318,#22319,#22320,#22321));
#6999=LINE('',#40452,#9868);
#7000=LINE('',#40463,#9869);
#9868=VECTOR('',#32228,1.);
#9869=VECTOR('',#32243,1.);
#10614=CIRCLE('',#26515,1.);
#10615=CIRCLE('',#26516,1.);
#10616=CIRCLE('',#26517,22.5);
#10617=CIRCLE('',#26518,1.);
#10618=CIRCLE('',#26519,1.);
#10619=CIRCLE('',#26521,1.);
#10620=CIRCLE('',#26522,1.);
#10621=CIRCLE('',#26524,22.5);
#10622=CIRCLE('',#26525,1.);
#10623=CIRCLE('',#26526,1.);
#12611=VERTEX_POINT('',#40441);
#12612=VERTEX_POINT('',#40442);
#12613=VERTEX_POINT('',#40445);
#12614=VERTEX_POINT('',#40447);
#12615=VERTEX_POINT('',#40451);
#12616=VERTEX_POINT('',#40453);
#12617=VERTEX_POINT('',#40457);
#12618=VERTEX_POINT('',#40459);
#15902=EDGE_CURVE('',#12611,#12612,#10614,.T.);
#15903=EDGE_CURVE('',#12612,#12611,#10615,.T.);
#15904=EDGE_CURVE('',#12612,#12613,#10616,.T.);
#15905=EDGE_CURVE('',#12613,#12614,#10617,.T.);
#15906=EDGE_CURVE('',#12614,#12613,#10618,.T.);
#15907=EDGE_CURVE('',#12614,#12615,#6999,.T.);
#15908=EDGE_CURVE('',#12615,#12616,#10619,.T.);
#15909=EDGE_CURVE('',#12616,#12615,#10620,.T.);
#15910=EDGE_CURVE('',#12616,#12617,#10621,.T.);
#15911=EDGE_CURVE('',#12617,#12618,#10622,.T.);
#15912=EDGE_CURVE('',#12618,#12617,#10623,.T.);
#15913=EDGE_CURVE('',#12618,#12611,#7000,.T.);
#22298=ORIENTED_EDGE('',*,*,#15902,.F.);
#22299=ORIENTED_EDGE('',*,*,#15903,.F.);
#22300=ORIENTED_EDGE('',*,*,#15904,.T.);
#22301=ORIENTED_EDGE('',*,*,#15905,.T.);
#22302=ORIENTED_EDGE('',*,*,#15906,.T.);
#22303=ORIENTED_EDGE('',*,*,#15904,.F.);
#22304=ORIENTED_EDGE('',*,*,#15906,.F.);
#22305=ORIENTED_EDGE('',*,*,#15907,.T.);
#22306=ORIENTED_EDGE('',*,*,#15908,.T.);
#22307=ORIENTED_EDGE('',*,*,#15909,.T.);
#22308=ORIENTED_EDGE('',*,*,#15907,.F.);
#22309=ORIENTED_EDGE('',*,*,#15905,.F.);
#22310=ORIENTED_EDGE('',*,*,#15908,.F.);
#22311=ORIENTED_EDGE('',*,*,#15909,.F.);
#22312=ORIENTED_EDGE('',*,*,#15910,.T.);
#22313=ORIENTED_EDGE('',*,*,#15911,.T.);
#22314=ORIENTED_EDGE('',*,*,#15912,.T.);
#22315=ORIENTED_EDGE('',*,*,#15910,.F.);
#22316=ORIENTED_EDGE('',*,*,#15912,.F.);
#22317=ORIENTED_EDGE('',*,*,#15913,.T.);
#22318=ORIENTED_EDGE('',*,*,#15902,.T.);
#22319=ORIENTED_EDGE('',*,*,#15903,.T.);
#22320=ORIENTED_EDGE('',*,*,#15913,.F.);
#22321=ORIENTED_EDGE('',*,*,#15911,.F.);
#24665=ADVANCED_FACE('',(#2806),#233,.T.);
#24666=ADVANCED_FACE('',(#2807),#530,.T.);
#24667=ADVANCED_FACE('',(#2808),#234,.T.);
#24668=ADVANCED_FACE('',(#2809),#531,.T.);
#24946=CLOSED_SHELL('',(#24665,#24666,#24667,#24668));
#26513=AXIS2_PLACEMENT_3D('',#40439,#32212,#32213);
#26514=AXIS2_PLACEMENT_3D('',#40440,#32214,#32215);
#26515=AXIS2_PLACEMENT_3D('',#40443,#32216,#32217);
#26516=AXIS2_PLACEMENT_3D('',#40444,#32218,#32219);
#26517=AXIS2_PLACEMENT_3D('',#40446,#32220,#32221);
#26518=AXIS2_PLACEMENT_3D('',#40448,#32222,#32223);
#26519=AXIS2_PLACEMENT_3D('',#40449,#32224,#32225);
#26520=AXIS2_PLACEMENT_3D('',#40450,#32226,#32227);
#26521=AXIS2_PLACEMENT_3D('',#40454,#32229,#32230);
#26522=AXIS2_PLACEMENT_3D('',#40455,#32231,#32232);
#26523=AXIS2_PLACEMENT_3D('',#40456,#32233,#32234);
#26524=AXIS2_PLACEMENT_3D('',#40458,#32235,#32236);
#26525=AXIS2_PLACEMENT_3D('',#40460,#32237,#32238);
#26526=AXIS2_PLACEMENT_3D('',#40461,#32239,#32240);
#26527=AXIS2_PLACEMENT_3D('',#40462,#32241,#32242);
#32212=DIRECTION('axis',(0.,0.,1.));
#32213=DIRECTION('refdir',(1.,0.,0.));
#32214=DIRECTION('center_axis',(0.,1.,0.));
#32215=DIRECTION('ref_axis',(0.,0.,1.));
#32216=DIRECTION('center_axis',(2.44929359829471E-16,0.,-1.));
#32217=DIRECTION('ref_axis',(2.22044604925031E-16,1.,5.43852429378756E-32));
#32218=DIRECTION('center_axis',(2.44929359829471E-16,0.,-1.));
#32219=DIRECTION('ref_axis',(2.22044604925031E-16,1.,5.43852429378756E-32));
#32220=DIRECTION('center_axis',(0.,-1.,0.));
#32221=DIRECTION('ref_axis',(0.,0.,1.));
#32222=DIRECTION('center_axis',(-1.22464679914735E-16,0.,1.));
#32223=DIRECTION('ref_axis',(-2.22044604925031E-16,1.,-2.71926214689378E-32));
#32224=DIRECTION('center_axis',(-1.22464679914735E-16,0.,1.));
#32225=DIRECTION('ref_axis',(-2.22044604925031E-16,1.,-2.71926214689378E-32));
#32226=DIRECTION('center_axis',(0.,0.,1.));
#32227=DIRECTION('ref_axis',(-2.22044604925031E-16,1.,0.));
#32228=DIRECTION('',(0.,0.,-1.));
#32229=DIRECTION('center_axis',(-1.22464679914735E-16,0.,1.));
#32230=DIRECTION('ref_axis',(-2.22044604925031E-16,1.,-2.71926214689378E-32));
#32231=DIRECTION('center_axis',(-1.22464679914735E-16,0.,1.));
#32232=DIRECTION('ref_axis',(-2.22044604925031E-16,1.,-2.71926214689378E-32));
#32233=DIRECTION('center_axis',(0.,1.,0.));
#32234=DIRECTION('ref_axis',(-1.22464679914735E-16,0.,-1.));
#32235=DIRECTION('center_axis',(0.,-1.,0.));
#32236=DIRECTION('ref_axis',(-1.22464679914735E-16,0.,-1.));
#32237=DIRECTION('center_axis',(0.,0.,-1.));
#32238=DIRECTION('ref_axis',(2.22044604925031E-16,1.,0.));
#32239=DIRECTION('center_axis',(0.,0.,-1.));
#32240=DIRECTION('ref_axis',(2.22044604925031E-16,1.,0.));
#32241=DIRECTION('center_axis',(0.,0.,-1.));
#32242=DIRECTION('ref_axis',(2.22044604925031E-16,1.,0.));
#32243=DIRECTION('',(0.,0.,1.));
#40439=CARTESIAN_POINT('',(0.,0.,0.));
#40440=CARTESIAN_POINT('Origin',(0.,17.,0.));
#40441=CARTESIAN_POINT('',(23.5,16.,7.31881207649691E-15));
#40442=CARTESIAN_POINT('',(22.5,17.,7.07388271666744E-15));
#40443=CARTESIAN_POINT('Origin',(23.5,17.,7.31881207649691E-15));
#40444=CARTESIAN_POINT('Origin',(23.5,17.,7.31881207649691E-15));
#40445=CARTESIAN_POINT('',(-22.5,17.,-4.31842741858589E-15));
#40446=CARTESIAN_POINT('Origin',(0.,17.,0.));
#40447=CARTESIAN_POINT('',(-23.5,16.,-4.44089209850063E-15));
#40448=CARTESIAN_POINT('Origin',(-23.5,17.,-4.44089209850063E-15));
#40449=CARTESIAN_POINT('Origin',(-23.5,17.,-4.44089209850063E-15));
#40450=CARTESIAN_POINT('Origin',(-23.5,17.,-33.));
#40451=CARTESIAN_POINT('',(-23.5,16.,-33.));
#40452=CARTESIAN_POINT('',(-23.5,16.,-33.));
#40453=CARTESIAN_POINT('',(-22.5,17.,-33.));
#40454=CARTESIAN_POINT('Origin',(-23.5,17.,-33.));
#40455=CARTESIAN_POINT('Origin',(-23.5,17.,-33.));
#40456=CARTESIAN_POINT('Origin',(0.,17.,-33.));
#40457=CARTESIAN_POINT('',(22.5,17.,-33.));
#40458=CARTESIAN_POINT('Origin',(0.,17.,-33.));
#40459=CARTESIAN_POINT('',(23.5,16.,-33.));
#40460=CARTESIAN_POINT('Origin',(23.5,17.,-33.));
#40461=CARTESIAN_POINT('Origin',(23.5,17.,-33.));
#40462=CARTESIAN_POINT('Origin',(23.5,17.,-16.5));
#40463=CARTESIAN_POINT('',(23.5,16.,-16.5));
#46374=UNCERTAINTY_MEASURE_WITH_UNIT(LENGTH_MEASURE(0.01),#46396,
'DISTANCE_ACCURACY_VALUE',
'Maximum model space distance between geometric entities at asserted c
onnectivities');
#46379=UNCERTAINTY_MEASURE_WITH_UNIT(LENGTH_MEASURE(0.01),#46396,
'DISTANCE_ACCURACY_VALUE',
'Maximum model space distance between geometric entities at asserted c
onnectivities');
#46390=(
GEOMETRIC_REPRESENTATION_CONTEXT(3)
GLOBAL_UNCERTAINTY_ASSIGNED_CONTEXT((#46374))
GLOBAL_UNIT_ASSIGNED_CONTEXT((#46396,#46398,#46399))
REPRESENTATION_CONTEXT('','3D')
);
#46395=(
GEOMETRIC_REPRESENTATION_CONTEXT(3)
GLOBAL_UNCERTAINTY_ASSIGNED_CONTEXT((#46379))
GLOBAL_UNIT_ASSIGNED_CONTEXT((#46396,#46398,#46399))
REPRESENTATION_CONTEXT('','3D')
);
#46396=(
LENGTH_UNIT()
NAMED_UNIT(*)
SI_UNIT(.MILLI.,.METRE.)
);
#46398=(
NAMED_UNIT(*)
PLANE_ANGLE_UNIT()
SI_UNIT($,.RADIAN.)
);
#46399=(
NAMED_UNIT(*)
SI_UNIT($,.STERADIAN.)
SOLID_ANGLE_UNIT()
);
#46410=SHAPE_DEFINITION_REPRESENTATION(#46425,#46465);
#46425=PRODUCT_DEFINITION_SHAPE('',$,#46481);
#46465=SHAPE_REPRESENTATION('',(#26513),#46390);
#46470=PRODUCT_DEFINITION_CONTEXT('part definition',#46517,'design');
#46481=PRODUCT_DEFINITION('2026-10-26-00-51-15-440',
'11_Body_Face_Seal_O-Ring',#46496,#46470);
#46496=PRODUCT_DEFINITION_FORMATION('',$,#46529);
#46517=APPLICATION_CONTEXT(
'Core Data for Automotive Mechanical Design Process');
#46518=PRODUCT_CONTEXT('part definition',#46517,'mechanical');
#46529=PRODUCT('2026-10-26-00-51-15-440','11_Body_Face_Seal_O-Ring',$,(#46518));
#46597=COLOUR_RGB('Black',0.12,0.14,0.17);
#46598=FILL_AREA_STYLE_COLOUR('',#46597);
#46599=FILL_AREA_STYLE('',(#46598));
#46600=SURFACE_STYLE_FILL_AREA(#46599);
#46601=SURFACE_SIDE_STYLE('',(#46600));
#46602=SURFACE_STYLE_USAGE(.BOTH.,#46601);
#46603=PRESENTATION_STYLE_ASSIGNMENT((#46602));
ENDSEC;
END-ISO-10303-21;
